ISO-10303-21;
HEADER;
/* Generated by software containing ST-Developer
 * from STEP Tools, Inc. (www.steptools.com) 
 */
/* OPTION: using custom renumber hook */

FILE_DESCRIPTION(
/* description */ ('STEP AP242 Edition 2', 'CAx-IF Rec.Pracs.---Representation and Presentation of Product Manufa
cturing Information (PMI)---4.0---2014-10-13', 'CAx-IF Rec.Pracs.---3D Tessellated Geometry---0.4---2014-09-14', '2;1', 'CAx-IF Rec.Pracs.---User Defined Attributes---1.5---2016-08-15'),
/* implementation_level */ '2;1');

FILE_NAME(
/* name */ 'Part 1.step',
/* time_stamp */ '2026-10-09T13:59:33Z',
/* author */ (''),
/* organization */ (''),
/* preprocessor_version */ 'ST-DEVELOPER v20',
/* originating_system */ 'ONSHAPE BY PTC INC, 1.221',
/* authorisation */ '  ');

FILE_SCHEMA (('AP242_MANAGED_MODEL_BASED_3D_ENGINEERING_MIM_LF { 1 0 10303 442 3 1 4 }'));
ENDSEC;

DATA;
#671=SHAPE_REPRESENTATION_RELATIONSHIP('','',#5689,#685);
#685=ADVANCED_BREP_SHAPE_REPRESENTATION('',(#5658),#10143);
#699=PLANE('',#5711);
#700=PLANE('',#5713);
#701=PLANE('',#5720);
#702=PLANE('',#5721);
#790=B_SPLINE_CURVE_WITH_KNOTS('',3,(#8397,#8398,#8399,#8400,#8401,#8402,
#8403,#8404,#8405,#8406,#8407),.UNSPECIFIED.,.T.,.F.,(1,1,1,1,1,1,1,1,1,
1,1,1,1,1,1),(-0.0117279316645703,-0.00781862110971355,-0.00390931055485677,
0.,0.00390931055485677,0.00781862110971355,0.0117279316645703,0.0156372422194271,
0.0195465527742839,0.0234558633291406,0.0273651738839974,0.0312744844388542,
0.035183794993711,0.0390931055485677,0.0430024161034245),.UNSPECIFIED.);
#791=B_SPLINE_CURVE_WITH_KNOTS('',3,(#8414,#8415,#8416,#8417,#8418,#8419,
#8420,#8421,#8422,#8423,#8424),.UNSPECIFIED.,.T.,.F.,(1,1,1,1,1,1,1,1,1,
1,1,1,1,1,1),(-0.0117277673344821,-0.00781851155632137,-0.00390925577816069,
0.,0.00390925577816069,0.00781851155632137,0.0117277673344821,0.0156370231126427,
0.0195462788908034,0.0234555346689641,0.0273647904471248,0.0312740462252855,
0.0351833020034462,0.0390925577816069,0.0430018135597676),.UNSPECIFIED.);
#814=ORIENTED_EDGE('',*,*,#2344,.T.);
#815=ORIENTED_EDGE('',*,*,#2345,.T.);
#816=ORIENTED_EDGE('',*,*,#2346,.T.);
#817=ORIENTED_EDGE('',*,*,#2347,.T.);
#818=ORIENTED_EDGE('',*,*,#2348,.F.);
#819=ORIENTED_EDGE('',*,*,#2349,.F.);
#820=ORIENTED_EDGE('',*,*,#2345,.F.);
#821=ORIENTED_EDGE('',*,*,#2350,.T.);
#822=ORIENTED_EDGE('',*,*,#2351,.T.);
#823=ORIENTED_EDGE('',*,*,#2352,.T.);
#824=ORIENTED_EDGE('',*,*,#2353,.T.);
#825=ORIENTED_EDGE('',*,*,#2354,.T.);
#826=ORIENTED_EDGE('',*,*,#2347,.F.);
#827=ORIENTED_EDGE('',*,*,#2355,.T.);
#828=ORIENTED_EDGE('',*,*,#2350,.F.);
#829=ORIENTED_EDGE('',*,*,#2348,.T.);
#830=ORIENTED_EDGE('',*,*,#2355,.F.);
#831=ORIENTED_EDGE('',*,*,#2356,.T.);
#832=ORIENTED_EDGE('',*,*,#2357,.T.);
#833=ORIENTED_EDGE('',*,*,#2358,.T.);
#834=ORIENTED_EDGE('',*,*,#2359,.T.);
#835=ORIENTED_EDGE('',*,*,#2344,.F.);
#836=ORIENTED_EDGE('',*,*,#2346,.F.);
#837=ORIENTED_EDGE('',*,*,#2349,.T.);
#838=ORIENTED_EDGE('',*,*,#2359,.F.);
#839=ORIENTED_EDGE('',*,*,#2354,.F.);
#840=ORIENTED_EDGE('',*,*,#2358,.F.);
#841=ORIENTED_EDGE('',*,*,#2353,.F.);
#842=ORIENTED_EDGE('',*,*,#2357,.F.);
#843=ORIENTED_EDGE('',*,*,#2352,.F.);
#844=ORIENTED_EDGE('',*,*,#2356,.F.);
#845=ORIENTED_EDGE('',*,*,#2351,.F.);
#2344=EDGE_CURVE('',#3109,#3109,#3650,.T.);
#2345=EDGE_CURVE('',#3110,#3110,#3651,.T.);
#2346=EDGE_CURVE('',#3111,#3111,#790,.T.);
#2347=EDGE_CURVE('',#3112,#3112,#3652,.T.);
#2348=EDGE_CURVE('',#3113,#3113,#3653,.T.);
#2349=EDGE_CURVE('',#3114,#3114,#791,.T.);
#2350=EDGE_CURVE('',#3115,#3115,#3654,.T.);
#2351=EDGE_CURVE('',#3116,#3116,#3655,.T.);
#2352=EDGE_CURVE('',#3117,#3117,#3656,.T.);
#2353=EDGE_CURVE('',#3118,#3118,#3657,.T.);
#2354=EDGE_CURVE('',#3119,#3119,#3658,.T.);
#2355=EDGE_CURVE('',#3120,#3120,#3659,.T.);
#2356=EDGE_CURVE('',#3121,#3121,#3660,.T.);
#2357=EDGE_CURVE('',#3122,#3122,#3661,.T.);
#2358=EDGE_CURVE('',#3123,#3123,#3662,.T.);
#2359=EDGE_CURVE('',#3124,#3124,#3663,.T.);
#3109=VERTEX_POINT('',#8394);
#3110=VERTEX_POINT('',#8396);
#3111=VERTEX_POINT('',#8408);
#3112=VERTEX_POINT('',#8411);
#3113=VERTEX_POINT('',#8413);
#3114=VERTEX_POINT('',#8425);
#3115=VERTEX_POINT('',#8428);
#3116=VERTEX_POINT('',#8431);
#3117=VERTEX_POINT('',#8433);
#3118=VERTEX_POINT('',#8435);
#3119=VERTEX_POINT('',#8437);
#3120=VERTEX_POINT('',#8440);
#3121=VERTEX_POINT('',#8444);
#3122=VERTEX_POINT('',#8446);
#3123=VERTEX_POINT('',#8448);
#3124=VERTEX_POINT('',#8450);
#3650=CIRCLE('',#5706,0.06);
#3651=CIRCLE('',#5707,0.06);
#3652=CIRCLE('',#5709,0.061);
#3653=CIRCLE('',#5710,0.061);
#3654=CIRCLE('',#5712,0.0635);
#3655=CIRCLE('',#5714,0.0015);
#3656=CIRCLE('',#5715,0.0015);
#3657=CIRCLE('',#5716,0.0015);
#3658=CIRCLE('',#5717,0.0015);
#3659=CIRCLE('',#5719,0.0635);
#3660=CIRCLE('',#5722,0.0015);
#3661=CIRCLE('',#5723,0.0015);
#3662=CIRCLE('',#5724,0.0015);
#3663=CIRCLE('',#5725,0.0015);
#4107=EDGE_LOOP('',(#814));
#4108=EDGE_LOOP('',(#815));
#4109=EDGE_LOOP('',(#816));
#4110=EDGE_LOOP('',(#817));
#4111=EDGE_LOOP('',(#818));
#4112=EDGE_LOOP('',(#819));
#4113=EDGE_LOOP('',(#820));
#4114=EDGE_LOOP('',(#821));
#4115=EDGE_LOOP('',(#822));
#4116=EDGE_LOOP('',(#823));
#4117=EDGE_LOOP('',(#824));
#4118=EDGE_LOOP('',(#825));
#4119=EDGE_LOOP('',(#826));
#4120=EDGE_LOOP('',(#827));
#4121=EDGE_LOOP('',(#828));
#4122=EDGE_LOOP('',(#829));
#4123=EDGE_LOOP('',(#830));
#4124=EDGE_LOOP('',(#831));
#4125=EDGE_LOOP('',(#832));
#4126=EDGE_LOOP('',(#833));
#4127=EDGE_LOOP('',(#834));
#4128=EDGE_LOOP('',(#835));
#4129=EDGE_LOOP('',(#836));
#4130=EDGE_LOOP('',(#837));
#4131=EDGE_LOOP('',(#838));
#4132=EDGE_LOOP('',(#839));
#4133=EDGE_LOOP('',(#840));
#4134=EDGE_LOOP('',(#841));
#4135=EDGE_LOOP('',(#842));
#4136=EDGE_LOOP('',(#843));
#4137=EDGE_LOOP('',(#844));
#4138=EDGE_LOOP('',(#845));
#4555=FACE_BOUND('',#4107,.T.);
#4556=FACE_BOUND('',#4108,.T.);
#4557=FACE_BOUND('',#4109,.T.);
#4558=FACE_BOUND('',#4110,.T.);
#4559=FACE_BOUND('',#4111,.T.);
#4560=FACE_BOUND('',#4112,.T.);
#4561=FACE_BOUND('',#4113,.T.);
#4562=FACE_BOUND('',#4114,.T.);
#4563=FACE_BOUND('',#4115,.T.);
#4564=FACE_BOUND('',#4116,.T.);
#4565=FACE_BOUND('',#4117,.T.);
#4566=FACE_BOUND('',#4118,.T.);
#4567=FACE_BOUND('',#4119,.T.);
#4568=FACE_BOUND('',#4120,.T.);
#4569=FACE_BOUND('',#4121,.T.);
#4570=FACE_BOUND('',#4122,.T.);
#4571=FACE_BOUND('',#4123,.T.);
#4572=FACE_BOUND('',#4124,.T.);
#4573=FACE_BOUND('',#4125,.T.);
#4574=FACE_BOUND('',#4126,.T.);
#4575=FACE_BOUND('',#4127,.T.);
#4576=FACE_BOUND('',#4128,.T.);
#4577=FACE_BOUND('',#4129,.T.);
#4578=FACE_BOUND('',#4130,.T.);
#4579=FACE_BOUND('',#4131,.T.);
#4580=FACE_BOUND('',#4132,.T.);
#4581=FACE_BOUND('',#4133,.T.);
#4582=FACE_BOUND('',#4134,.T.);
#4583=FACE_BOUND('',#4135,.T.);
#4584=FACE_BOUND('',#4136,.T.);
#4585=FACE_BOUND('',#4137,.T.);
#4586=FACE_BOUND('',#4138,.T.);
#5003=CYLINDRICAL_SURFACE('',#5705,0.06);
#5004=CYLINDRICAL_SURFACE('',#5708,0.061);
#5005=CYLINDRICAL_SURFACE('',#5718,0.0635);
#5006=CYLINDRICAL_SURFACE('',#5726,0.005);
#5007=CYLINDRICAL_SURFACE('',#5727,0.0015);
#5008=CYLINDRICAL_SURFACE('',#5728,0.0015);
#5009=CYLINDRICAL_SURFACE('',#5729,0.0015);
#5010=CYLINDRICAL_SURFACE('',#5730,0.0015);
#5213=ADVANCED_FACE('',(#4555,#4556,#4557),#5003,.F.);
#5214=ADVANCED_FACE('',(#4558,#4559,#4560),#5004,.T.);
#5215=ADVANCED_FACE('',(#4561,#4562),#699,.T.);
#5216=ADVANCED_FACE('',(#4563,#4564,#4565,#4566,#4567),#700,.F.);
#5217=ADVANCED_FACE('',(#4568,#4569),#5005,.T.);
#5218=ADVANCED_FACE('',(#4570,#4571),#701,.F.);
#5219=ADVANCED_FACE('',(#4572,#4573,#4574,#4575,#4576),#702,.F.);
#5220=ADVANCED_FACE('',(#4577,#4578),#5006,.F.);
#5221=ADVANCED_FACE('',(#4579,#4580),#5007,.F.);
#5222=ADVANCED_FACE('',(#4581,#4582),#5008,.F.);
#5223=ADVANCED_FACE('',(#4583,#4584),#5009,.F.);
#5224=ADVANCED_FACE('',(#4585,#4586),#5010,.F.);
#5539=CLOSED_SHELL('',(#5213,#5214,#5215,#5216,#5217,#5218,#5219,#5220,
#5221,#5222,#5223,#5224));
#5553=STYLED_ITEM('',(#5567),#5658);
#5567=PRESENTATION_STYLE_ASSIGNMENT((#5581));
#5581=SURFACE_STYLE_USAGE(.BOTH.,#5595);
#5595=SURFACE_SIDE_STYLE('',(#5609));
#5609=SURFACE_STYLE_FILL_AREA(#5623);
#5623=FILL_AREA_STYLE('',(#5637));
#5637=FILL_AREA_STYLE_COLOUR('',#5651);
#5651=COLOUR_RGB('', 0.66274510, 0.83137255, 0.94901961);
#5658=MANIFOLD_SOLID_BREP('Part 1',#5539);
#5673=SHAPE_DEFINITION_REPRESENTATION(#10178,#5689);
#5689=SHAPE_REPRESENTATION('Part 1',(#5704),#10143);
#5704=AXIS2_PLACEMENT_3D('',#8391,#6505,#6506);
#5705=AXIS2_PLACEMENT_3D('',#8392,#6507,#6508);
#5706=AXIS2_PLACEMENT_3D('',#8393,#6509,#6510);
#5707=AXIS2_PLACEMENT_3D('',#8395,#6511,#6512);
#5708=AXIS2_PLACEMENT_3D('',#8409,#6513,#6514);
#5709=AXIS2_PLACEMENT_3D('',#8410,#6515,#6516);
#5710=AXIS2_PLACEMENT_3D('',#8412,#6517,#6518);
#5711=AXIS2_PLACEMENT_3D('',#8426,#6519,#6520);
#5712=AXIS2_PLACEMENT_3D('',#8427,#6521,#6522);
#5713=AXIS2_PLACEMENT_3D('',#8429,#6523,#6524);
#5714=AXIS2_PLACEMENT_3D('',#8430,#6525,#6526);
#5715=AXIS2_PLACEMENT_3D('',#8432,#6527,#6528);
#5716=AXIS2_PLACEMENT_3D('',#8434,#6529,#6530);
#5717=AXIS2_PLACEMENT_3D('',#8436,#6531,#6532);
#5718=AXIS2_PLACEMENT_3D('',#8438,#6533,#6534);
#5719=AXIS2_PLACEMENT_3D('',#8439,#6535,#6536);
#5720=AXIS2_PLACEMENT_3D('',#8441,#6537,#6538);
#5721=AXIS2_PLACEMENT_3D('',#8442,#6539,#6540);
#5722=AXIS2_PLACEMENT_3D('',#8443,#6541,#6542);
#5723=AXIS2_PLACEMENT_3D('',#8445,#6543,#6544);
#5724=AXIS2_PLACEMENT_3D('',#8447,#6545,#6546);
#5725=AXIS2_PLACEMENT_3D('',#8449,#6547,#6548);
#5726=AXIS2_PLACEMENT_3D('',#8451,#6549,#6550);
#5727=AXIS2_PLACEMENT_3D('',#8452,#6551,#6552);
#5728=AXIS2_PLACEMENT_3D('',#8453,#6553,#6554);
#5729=AXIS2_PLACEMENT_3D('',#8454,#6555,#6556);
#5730=AXIS2_PLACEMENT_3D('',#8455,#6557,#6558);
#6505=DIRECTION('',(0.,0.,1.));
#6506=DIRECTION('',(1.,0.,0.));
#6507=DIRECTION('',(0.,-1.,0.));
#6508=DIRECTION('',(0.,0.,-1.));
#6509=DIRECTION('',(0.,-1.,0.));
#6510=DIRECTION('',(0.,0.,-1.));
#6511=DIRECTION('',(0.,1.,0.));
#6512=DIRECTION('',(0.,0.,1.));
#6513=DIRECTION('',(0.,-1.,0.));
#6514=DIRECTION('',(0.,0.,-1.));
#6515=DIRECTION('',(0.,1.,0.));
#6516=DIRECTION('',(1.,0.,0.));
#6517=DIRECTION('',(0.,1.,0.));
#6518=DIRECTION('',(0.,0.,1.));
#6519=DIRECTION('',(0.,1.,0.));
#6520=DIRECTION('',(0.,0.,1.));
#6521=DIRECTION('',(0.,1.,0.));
#6522=DIRECTION('',(0.,0.,1.));
#6523=DIRECTION('',(0.,1.,0.));
#6524=DIRECTION('',(0.,0.,1.));
#6525=DIRECTION('',(0.,1.,0.));
#6526=DIRECTION('',(0.,0.,1.));
#6527=DIRECTION('',(0.,1.,0.));
#6528=DIRECTION('',(0.,0.,1.));
#6529=DIRECTION('',(0.,1.,0.));
#6530=DIRECTION('',(0.,0.,1.));
#6531=DIRECTION('',(0.,1.,0.));
#6532=DIRECTION('',(0.,0.,1.));
#6533=DIRECTION('',(0.,1.,0.));
#6534=DIRECTION('',(0.,0.,1.));
#6535=DIRECTION('',(0.,1.,0.));
#6536=DIRECTION('',(0.,0.,1.));
#6537=DIRECTION('',(0.,1.,0.));
#6538=DIRECTION('',(0.,0.,1.));
#6539=DIRECTION('',(0.,-1.,0.));
#6540=DIRECTION('',(0.,0.,-1.));
#6541=DIRECTION('',(0.,-1.,0.));
#6542=DIRECTION('',(0.,0.,-1.));
#6543=DIRECTION('',(0.,-1.,0.));
#6544=DIRECTION('',(0.,0.,-1.));
#6545=DIRECTION('',(0.,-1.,0.));
#6546=DIRECTION('',(0.,0.,-1.));
#6547=DIRECTION('',(0.,-1.,0.));
#6548=DIRECTION('',(0.,0.,-1.));
#6549=DIRECTION('',(0.,0.,-1.));
#6550=DIRECTION('',(-1.,0.,0.));
#6551=DIRECTION('',(0.,1.,0.));
#6552=DIRECTION('',(0.,0.,1.));
#6553=DIRECTION('',(0.,1.,0.));
#6554=DIRECTION('',(0.,0.,1.));
#6555=DIRECTION('',(0.,1.,0.));
#6556=DIRECTION('',(0.,0.,1.));
#6557=DIRECTION('',(0.,1.,0.));
#6558=DIRECTION('',(0.,0.,1.));
#8391=CARTESIAN_POINT('',(0.,0.,0.));
#8392=CARTESIAN_POINT('',(0.,0.03,0.));
#8393=CARTESIAN_POINT('',(0.,0.001,0.));
#8394=CARTESIAN_POINT('',(0.,0.001,-0.06));
#8395=CARTESIAN_POINT('',(0.,0.03,0.));
#8396=CARTESIAN_POINT('',(0.,0.03,0.06));
#8397=CARTESIAN_POINT('',(-0.0039149404887588,0.0139224634434835,0.0598960985083079));
#8398=CARTESIAN_POINT('',(-0.00554222253988876,0.00999901026546572,0.0597389564762431));
#8399=CARTESIAN_POINT('',(-0.00391616935168617,0.00608149549465367,0.0598958978797615));
#8400=CARTESIAN_POINT('',(-4.23543574001425E-6,0.00445973646869292,0.0600520305933898));
#8401=CARTESIAN_POINT('',(0.00391685859097665,0.00607956303297287,0.0598959793798127));
#8402=CARTESIAN_POINT('',(0.00554029535879261,0.00999910325696514,0.0597390813899988));
#8403=CARTESIAN_POINT('',(0.00392195799437461,0.0139131258340931,0.0598955175187662));
#8404=CARTESIAN_POINT('',(5.55403455442611E-6,0.015541099119747,0.0600520956964933));
#8405=CARTESIAN_POINT('',(-0.0039149404887588,0.0139224634434835,0.0598960985083079));
#8406=CARTESIAN_POINT('',(-0.00554222253988876,0.00999901026546572,0.0597389564762431));
#8407=CARTESIAN_POINT('',(-0.00391616935168617,0.00608149549465367,0.0598958978797615));
#8408=CARTESIAN_POINT('',(-0.005,0.01,0.059791303715507));
#8409=CARTESIAN_POINT('',(0.,0.03,0.));
#8410=CARTESIAN_POINT('',(0.,0.,0.));
#8411=CARTESIAN_POINT('',(0.061,0.,0.));
#8412=CARTESIAN_POINT('',(0.,0.029,0.));
#8413=CARTESIAN_POINT('',(0.,0.029,0.061));
#8414=CARTESIAN_POINT('',(-0.00391494265834519,0.0139224651131911,0.0608978018788975));
#8415=CARTESIAN_POINT('',(-0.00554222119578978,0.00999900968220688,0.060743253346584));
#8416=CARTESIAN_POINT('',(-0.00391617255849569,0.0060814961579814,0.0608976044204628));
#8417=CARTESIAN_POINT('',(-4.2288777227757E-6,0.0044597393228037,0.061051177490022));
#8418=CARTESIAN_POINT('',(0.00391684609381935,0.0060795509475003,0.0608976852590645));
#8419=CARTESIAN_POINT('',(0.00554029932935669,0.00999910932086652,0.0607433760647901));
#8420=CARTESIAN_POINT('',(0.00392195461275095,0.013913123234971,0.0608972303299854));
#8421=CARTESIAN_POINT('',(5.56769475100309E-6,0.0155410993401316,0.0610512416549246));
#8422=CARTESIAN_POINT('',(-0.00391494265834519,0.0139224651131911,0.0608978018788975));
#8423=CARTESIAN_POINT('',(-0.00554222119578978,0.00999900968220688,0.060743253346584));
#8424=CARTESIAN_POINT('',(-0.00391617255849569,0.0060814961579814,0.0608976044204628));
#8425=CARTESIAN_POINT('',(-0.005,0.01,0.0607947366142827));
#8426=CARTESIAN_POINT('',(0.,0.03,0.));
#8427=CARTESIAN_POINT('',(0.,0.03,0.));
#8428=CARTESIAN_POINT('',(0.,0.03,0.0635));
#8429=CARTESIAN_POINT('',(0.,0.,0.));
#8430=CARTESIAN_POINT('',(-0.0135975206449919,0.,0.0124363480647457));
#8431=CARTESIAN_POINT('',(-0.0135975206449919,0.,0.0139363480647457));
#8432=CARTESIAN_POINT('',(-0.00538454930157943,0.,0.0176227679351839));
#8433=CARTESIAN_POINT('',(-0.00538454930157943,0.,0.0191227679351839));
#8434=CARTESIAN_POINT('',(0.00427564662218917,0.,0.00232533458508421));
#8435=CARTESIAN_POINT('',(0.00427564662218917,0.,0.00382533458508421));
#8436=CARTESIAN_POINT('',(-0.00393732472122328,0.,-0.00286108528535397));
#8437=CARTESIAN_POINT('',(-0.00393732472122328,0.,-0.00136108528535397));
#8438=CARTESIAN_POINT('',(0.,0.029,0.));
#8439=CARTESIAN_POINT('',(0.,0.029,0.));
#8440=CARTESIAN_POINT('',(0.,0.029,0.0635));
#8441=CARTESIAN_POINT('',(0.,0.029,0.));
#8442=CARTESIAN_POINT('',(0.,0.001,0.));
#8443=CARTESIAN_POINT('',(-0.0135975206449919,0.001,0.0124363480647457));
#8444=CARTESIAN_POINT('',(-0.0135975206449919,0.001,0.0109363480647457));
#8445=CARTESIAN_POINT('',(-0.00538454930157943,0.001,0.0176227679351839));
#8446=CARTESIAN_POINT('',(-0.00538454930157943,0.001,0.0161227679351839));
#8447=CARTESIAN_POINT('',(0.00427564662218917,0.001,0.00232533458508421));
#8448=CARTESIAN_POINT('',(0.00427564662218917,0.001,0.000825334585084205));
#8449=CARTESIAN_POINT('',(-0.00393732472122328,0.001,-0.00286108528535397));
#8450=CARTESIAN_POINT('',(-0.00393732472122328,0.001,-0.00436108528535397));
#8451=CARTESIAN_POINT('',(2.32682891837997E-18,0.01,0.124));
#8452=CARTESIAN_POINT('',(-0.00393732472122328,-0.181103382636493,-0.00286108528535397));
#8453=CARTESIAN_POINT('',(0.00427564662218917,-0.181103382636493,0.00232533458508421));
#8454=CARTESIAN_POINT('',(-0.00538454930157943,-0.181103382636493,0.0176227679351839));
#8455=CARTESIAN_POINT('',(-0.0135975206449919,-0.181103382636493,0.0124363480647457));
#10141=MECHANICAL_DESIGN_GEOMETRIC_PRESENTATION_REPRESENTATION('',(#5553),#10142);
#10142=(
GEOMETRIC_REPRESENTATION_CONTEXT(3)
GLOBAL_UNCERTAINTY_ASSIGNED_CONTEXT((#10158))
GLOBAL_UNIT_ASSIGNED_CONTEXT((#10176,#10175,#10174))
REPRESENTATION_CONTEXT('MAS-674','TOP_LEVEL_ASSEMBLY_PART')
);
#10143=(
GEOMETRIC_REPRESENTATION_CONTEXT(3)
GLOBAL_UNCERTAINTY_ASSIGNED_CONTEXT((#10159))
GLOBAL_UNIT_ASSIGNED_CONTEXT((#10176,#10175,#10174))
REPRESENTATION_CONTEXT('Part 1','COMPONENT_PART')
);
#10158=UNCERTAINTY_MEASURE_WITH_UNIT(LENGTH_MEASURE(1.E-8),#10176,
'DISTANCE_ACCURACY_VALUE','Maximum Tolerance applied to model');
#10159=UNCERTAINTY_MEASURE_WITH_UNIT(LENGTH_MEASURE(2.E-5),#10176,
'DISTANCE_ACCURACY_VALUE','Maximum Tolerance applied to model');
#10174=(
NAMED_UNIT(*)
SI_UNIT($,.STERADIAN.)
SOLID_ANGLE_UNIT()
);
#10175=(
NAMED_UNIT(*)
PLANE_ANGLE_UNIT()
SI_UNIT($,.RADIAN.)
);
#10176=(
LENGTH_UNIT()
NAMED_UNIT(*)
SI_UNIT($,.METRE.)
);
#10178=PRODUCT_DEFINITION_SHAPE('','',#10211);
#10211=PRODUCT_DEFINITION('','',#10243,#10227);
#10227=PRODUCT_DEFINITION_CONTEXT('',#10323,'design');
#10243=PRODUCT_DEFINITION_FORMATION_WITH_SPECIFIED_SOURCE('','',#10275,
 .NOT_KNOWN.);
#10275=PRODUCT('Part 1','Part 1','Part 1',(#10307));
#10307=PRODUCT_CONTEXT('',#10323,'mechanical');
#10323=APPLICATION_CONTEXT('managed model based 3d engineering');
ENDSEC;
END-ISO-10303-21;
